ISO-10303-21;
HEADER;
/* Generated by software containing ST-Developer
 * from STEP Tools, Inc. (www.steptools.com) 
 */

FILE_DESCRIPTION(
/* description */ ('PAT-054'),
/* implementation_level */ '2;1');

FILE_NAME(
/* name */ 'M5x18 runner screw.step',
/* time_stamp */ '2026-10-29T16:38:13-07:00',
/* author */ (''),
/* organization */ (''),
/* preprocessor_version */ 'ST-DEVELOPER v20.2',
/* originating_system */ 'Autodesk Translation Framework v15.17.0.0',
/* authorisation */ '');

FILE_SCHEMA (('AUTOMOTIVE_DESIGN { 1 0 10303 214 3 1 1 }'));
ENDSEC;

DATA;
#10=MECHANICAL_DESIGN_GEOMETRIC_PRESENTATION_REPRESENTATION('',(#936),#33981);
#15=ORIENTED_CLOSED_SHELL('',*,#13047,.F.);
#20=BREP_WITH_VOIDS('Body1',#13048,(#15));
#786=CONICAL_SURFACE('',#14224,0.4,0.785398163397448);
#787=CONICAL_SURFACE('',#14228,0.41,0.785398163397448);
#788=CONICAL_SURFACE('',#14232,0.26,0.463647609000806);
#833=SHAPE_REPRESENTATION_RELATIONSHIP('SRR','None',#34208,#877);
#877=ADVANCED_BREP_SHAPE_REPRESENTATION('',(#20),#33956);
#936=STYLED_ITEM('',(#34524),#20);
#1151=FACE_BOUND('',#2765,.T.);
#1401=PLANE('',#14212);
#1402=PLANE('',#14213);
#1403=PLANE('',#14214);
#1404=PLANE('',#14215);
#1405=PLANE('',#14216);
#1406=PLANE('',#14217);
#1407=PLANE('',#14218);
#1408=PLANE('',#14219);
#1409=PLANE('',#14220);
#1410=PLANE('',#14222);
#1411=PLANE('',#14230);
#1889=FACE_OUTER_BOUND('',#2751,.T.);
#1890=FACE_OUTER_BOUND('',#2752,.T.);
#1891=FACE_OUTER_BOUND('',#2753,.T.);
#1892=FACE_OUTER_BOUND('',#2754,.T.);
#1893=FACE_OUTER_BOUND('',#2755,.T.);
#1894=FACE_OUTER_BOUND('',#2756,.T.);
#1895=FACE_OUTER_BOUND('',#2757,.T.);
#1896=FACE_OUTER_BOUND('',#2758,.T.);
#1897=FACE_OUTER_BOUND('',#2759,.T.);
#1898=FACE_OUTER_BOUND('',#2760,.T.);
#1899=FACE_OUTER_BOUND('',#2761,.T.);
#1900=FACE_OUTER_BOUND('',#2762,.T.);
#1901=FACE_OUTER_BOUND('',#2763,.T.);
#1902=FACE_OUTER_BOUND('',#2764,.T.);
#1903=FACE_OUTER_BOUND('',#2766,.T.);
#1904=FACE_OUTER_BOUND('',#2767,.T.);
#2751=EDGE_LOOP('',(#9977,#9978,#9979,#9980));
#2752=EDGE_LOOP('',(#9981,#9982,#9983,#9984));
#2753=EDGE_LOOP('',(#9985,#9986,#9987,#9988));
#2754=EDGE_LOOP('',(#9989,#9990,#9991,#9992));
#2755=EDGE_LOOP('',(#9993,#9994,#9995,#9996));
#2756=EDGE_LOOP('',(#9997,#9998,#9999,#10000));
#2757=EDGE_LOOP('',(#10001,#10002,#10003,#10004,#10005,#10006));
#2758=EDGE_LOOP('',(#10007,#10008,#10009,#10010,#10011,#10012));
#2759=EDGE_LOOP('',(#10013));
#2760=EDGE_LOOP('',(#10014));
#2761=EDGE_LOOP('',(#10015,#10016,#10017,#10018));
#2762=EDGE_LOOP('',(#10019,#10020,#10021,#10022));
#2763=EDGE_LOOP('',(#10023,#10024,#10025,#10026));
#2764=EDGE_LOOP('',(#10027));
#2765=EDGE_LOOP('',(#10028));
#2766=EDGE_LOOP('',(#10029,#10030,#10031,#10032));
#2767=EDGE_LOOP('',(#10033,#10034,#10035,#10036));
#3647=LINE('',#20729,#4581);
#3648=LINE('',#20731,#4582);
#3649=LINE('',#20733,#4583);
#3650=LINE('',#20734,#4584);
#3651=LINE('',#20737,#4585);
#3652=LINE('',#20739,#4586);
#3653=LINE('',#20740,#4587);
#3654=LINE('',#20743,#4588);
#3655=LINE('',#20745,#4589);
#3656=LINE('',#20746,#4590);
#3657=LINE('',#20749,#4591);
#3658=LINE('',#20751,#4592);
#3659=LINE('',#20752,#4593);
#3660=LINE('',#20755,#4594);
#3661=LINE('',#20757,#4595);
#3662=LINE('',#20758,#4596);
#3663=LINE('',#20760,#4597);
#3664=LINE('',#20761,#4598);
#3665=LINE('',#20773,#4599);
#3666=LINE('',#20777,#4600);
#3667=LINE('',#20781,#4601);
#3668=LINE('',#20788,#4602);
#3669=LINE('',#20790,#4603);
#4581=VECTOR('',#16608,1.);
#4582=VECTOR('',#16609,1.);
#4583=VECTOR('',#16610,1.);
#4584=VECTOR('',#16611,1.);
#4585=VECTOR('',#16614,1.);
#4586=VECTOR('',#16615,1.);
#4587=VECTOR('',#16616,1.);
#4588=VECTOR('',#16619,1.);
#4589=VECTOR('',#16620,1.);
#4590=VECTOR('',#16621,1.);
#4591=VECTOR('',#16624,1.);
#4592=VECTOR('',#16625,1.);
#4593=VECTOR('',#16626,1.);
#4594=VECTOR('',#16629,1.);
#4595=VECTOR('',#16630,1.);
#4596=VECTOR('',#16631,1.);
#4597=VECTOR('',#16634,1.);
#4598=VECTOR('',#16635,1.);
#4599=VECTOR('',#16652,0.4);
#4600=VECTOR('',#16657,0.425);
#4601=VECTOR('',#16662,0.41);
#4602=VECTOR('',#16671,0.26);
#4603=VECTOR('',#16674,0.25);
#5405=CIRCLE('',#14221,0.24505);
#5406=CIRCLE('',#14223,0.375);
#5407=CIRCLE('',#14225,0.425);
#5408=CIRCLE('',#14227,0.425);
#5409=CIRCLE('',#14229,0.395);
#5410=CIRCLE('',#14231,0.27);
#5411=CIRCLE('',#14233,0.24505);
#6083=VERTEX_POINT('',#20727);
#6084=VERTEX_POINT('',#20728);
#6085=VERTEX_POINT('',#20730);
#6086=VERTEX_POINT('',#20732);
#6087=VERTEX_POINT('',#20736);
#6088=VERTEX_POINT('',#20738);
#6089=VERTEX_POINT('',#20742);
#6090=VERTEX_POINT('',#20744);
#6091=VERTEX_POINT('',#20748);
#6092=VERTEX_POINT('',#20750);
#6093=VERTEX_POINT('',#20754);
#6094=VERTEX_POINT('',#20756);
#6095=VERTEX_POINT('',#20765);
#6096=VERTEX_POINT('',#20768);
#6097=VERTEX_POINT('',#20771);
#6098=VERTEX_POINT('',#20775);
#6099=VERTEX_POINT('',#20779);
#6100=VERTEX_POINT('',#20783);
#6101=VERTEX_POINT('',#20786);
#7488=EDGE_CURVE('',#6083,#6084,#3647,.T.);
#7489=EDGE_CURVE('',#6084,#6085,#3648,.T.);
#7490=EDGE_CURVE('',#6085,#6086,#3649,.T.);
#7491=EDGE_CURVE('',#6083,#6086,#3650,.T.);
#7492=EDGE_CURVE('',#6084,#6087,#3651,.T.);
#7493=EDGE_CURVE('',#6087,#6088,#3652,.T.);
#7494=EDGE_CURVE('',#6088,#6085,#3653,.T.);
#7495=EDGE_CURVE('',#6087,#6089,#3654,.T.);
#7496=EDGE_CURVE('',#6089,#6090,#3655,.T.);
#7497=EDGE_CURVE('',#6090,#6088,#3656,.T.);
#7498=EDGE_CURVE('',#6089,#6091,#3657,.T.);
#7499=EDGE_CURVE('',#6091,#6092,#3658,.T.);
#7500=EDGE_CURVE('',#6092,#6090,#3659,.T.);
#7501=EDGE_CURVE('',#6091,#6093,#3660,.T.);
#7502=EDGE_CURVE('',#6093,#6094,#3661,.T.);
#7503=EDGE_CURVE('',#6094,#6092,#3662,.T.);
#7504=EDGE_CURVE('',#6093,#6083,#3663,.T.);
#7505=EDGE_CURVE('',#6086,#6094,#3664,.T.);
#7506=EDGE_CURVE('',#6095,#6095,#5405,.T.);
#7507=EDGE_CURVE('',#6096,#6096,#5406,.T.);
#7508=EDGE_CURVE('',#6097,#6097,#5407,.T.);
#7509=EDGE_CURVE('',#6097,#6096,#3665,.T.);
#7510=EDGE_CURVE('',#6098,#6098,#5408,.T.);
#7511=EDGE_CURVE('',#6098,#6097,#3666,.T.);
#7512=EDGE_CURVE('',#6099,#6099,#5409,.T.);
#7513=EDGE_CURVE('',#6099,#6098,#3667,.T.);
#7514=EDGE_CURVE('',#6100,#6100,#5410,.T.);
#7515=EDGE_CURVE('',#6101,#6101,#5411,.F.);
#7516=EDGE_CURVE('',#6101,#6100,#3668,.T.);
#7517=EDGE_CURVE('',#6095,#6101,#3669,.T.);
#9977=ORIENTED_EDGE('',*,*,#7488,.T.);
#9978=ORIENTED_EDGE('',*,*,#7489,.T.);
#9979=ORIENTED_EDGE('',*,*,#7490,.T.);
#9980=ORIENTED_EDGE('',*,*,#7491,.F.);
#9981=ORIENTED_EDGE('',*,*,#7492,.T.);
#9982=ORIENTED_EDGE('',*,*,#7493,.T.);
#9983=ORIENTED_EDGE('',*,*,#7494,.T.);
#9984=ORIENTED_EDGE('',*,*,#7489,.F.);
#9985=ORIENTED_EDGE('',*,*,#7495,.T.);
#9986=ORIENTED_EDGE('',*,*,#7496,.T.);
#9987=ORIENTED_EDGE('',*,*,#7497,.T.);
#9988=ORIENTED_EDGE('',*,*,#7493,.F.);
#9989=ORIENTED_EDGE('',*,*,#7498,.T.);
#9990=ORIENTED_EDGE('',*,*,#7499,.T.);
#9991=ORIENTED_EDGE('',*,*,#7500,.T.);
#9992=ORIENTED_EDGE('',*,*,#7496,.F.);
#9993=ORIENTED_EDGE('',*,*,#7501,.T.);
#9994=ORIENTED_EDGE('',*,*,#7502,.T.);
#9995=ORIENTED_EDGE('',*,*,#7503,.T.);
#9996=ORIENTED_EDGE('',*,*,#7499,.F.);
#9997=ORIENTED_EDGE('',*,*,#7504,.T.);
#9998=ORIENTED_EDGE('',*,*,#7491,.T.);
#9999=ORIENTED_EDGE('',*,*,#7505,.T.);
#10000=ORIENTED_EDGE('',*,*,#7502,.F.);
#10001=ORIENTED_EDGE('',*,*,#7504,.F.);
#10002=ORIENTED_EDGE('',*,*,#7501,.F.);
#10003=ORIENTED_EDGE('',*,*,#7498,.F.);
#10004=ORIENTED_EDGE('',*,*,#7495,.F.);
#10005=ORIENTED_EDGE('',*,*,#7492,.F.);
#10006=ORIENTED_EDGE('',*,*,#7488,.F.);
#10007=ORIENTED_EDGE('',*,*,#7505,.F.);
#10008=ORIENTED_EDGE('',*,*,#7490,.F.);
#10009=ORIENTED_EDGE('',*,*,#7494,.F.);
#10010=ORIENTED_EDGE('',*,*,#7497,.F.);
#10011=ORIENTED_EDGE('',*,*,#7500,.F.);
#10012=ORIENTED_EDGE('',*,*,#7503,.F.);
#10013=ORIENTED_EDGE('',*,*,#7506,.F.);
#10014=ORIENTED_EDGE('',*,*,#7507,.F.);
#10015=ORIENTED_EDGE('',*,*,#7508,.F.);
#10016=ORIENTED_EDGE('',*,*,#7509,.T.);
#10017=ORIENTED_EDGE('',*,*,#7507,.T.);
#10018=ORIENTED_EDGE('',*,*,#7509,.F.);
#10019=ORIENTED_EDGE('',*,*,#7510,.F.);
#10020=ORIENTED_EDGE('',*,*,#7511,.T.);
#10021=ORIENTED_EDGE('',*,*,#7508,.T.);
#10022=ORIENTED_EDGE('',*,*,#7511,.F.);
#10023=ORIENTED_EDGE('',*,*,#7512,.F.);
#10024=ORIENTED_EDGE('',*,*,#7513,.T.);
#10025=ORIENTED_EDGE('',*,*,#7510,.T.);
#10026=ORIENTED_EDGE('',*,*,#7513,.F.);
#10027=ORIENTED_EDGE('',*,*,#7512,.T.);
#10028=ORIENTED_EDGE('',*,*,#7514,.F.);
#10029=ORIENTED_EDGE('',*,*,#7515,.F.);
#10030=ORIENTED_EDGE('',*,*,#7516,.T.);
#10031=ORIENTED_EDGE('',*,*,#7514,.T.);
#10032=ORIENTED_EDGE('',*,*,#7516,.F.);
#10033=ORIENTED_EDGE('',*,*,#7506,.T.);
#10034=ORIENTED_EDGE('',*,*,#7517,.T.);
#10035=ORIENTED_EDGE('',*,*,#7515,.T.);
#10036=ORIENTED_EDGE('',*,*,#7517,.F.);
#12077=CYLINDRICAL_SURFACE('',#14226,0.425);
#12078=CYLINDRICAL_SURFACE('',#14234,0.24505);
#12601=ADVANCED_FACE('',(#1889),#1401,.F.);
#12602=ADVANCED_FACE('',(#1890),#1402,.F.);
#12603=ADVANCED_FACE('',(#1891),#1403,.F.);
#12604=ADVANCED_FACE('',(#1892),#1404,.F.);
#12605=ADVANCED_FACE('',(#1893),#1405,.F.);
#12606=ADVANCED_FACE('',(#1894),#1406,.F.);
#12607=ADVANCED_FACE('',(#1895),#1407,.F.);
#12608=ADVANCED_FACE('',(#1896),#1408,.F.);
#12609=ADVANCED_FACE('',(#1897),#1409,.F.);
#12610=ADVANCED_FACE('',(#1898),#1410,.T.);
#12611=ADVANCED_FACE('',(#1899),#786,.T.);
#12612=ADVANCED_FACE('',(#1900),#12077,.T.);
#12613=ADVANCED_FACE('',(#1901),#787,.T.);
#12614=ADVANCED_FACE('',(#1902,#1151),#1411,.T.);
#12615=ADVANCED_FACE('',(#1903),#788,.T.);
#12616=ADVANCED_FACE('',(#1904),#12078,.T.);
#13047=CLOSED_SHELL('',(#12601,#12602,#12603,#12604,#12605,#12606,#12607,
#12608));
#13048=CLOSED_SHELL('',(#12609,#12610,#12611,#12612,#12613,#12614,#12615,
#12616));
#14211=AXIS2_PLACEMENT_3D('',#20725,#16604,#16605);
#14212=AXIS2_PLACEMENT_3D('',#20726,#16606,#16607);
#14213=AXIS2_PLACEMENT_3D('',#20735,#16612,#16613);
#14214=AXIS2_PLACEMENT_3D('',#20741,#16617,#16618);
#14215=AXIS2_PLACEMENT_3D('',#20747,#16622,#16623);
#14216=AXIS2_PLACEMENT_3D('',#20753,#16627,#16628);
#14217=AXIS2_PLACEMENT_3D('',#20759,#16632,#16633);
#14218=AXIS2_PLACEMENT_3D('',#20762,#16636,#16637);
#14219=AXIS2_PLACEMENT_3D('',#20763,#16638,#16639);
#14220=AXIS2_PLACEMENT_3D('',#20764,#16640,#16641);
#14221=AXIS2_PLACEMENT_3D('',#20766,#16642,#16643);
#14222=AXIS2_PLACEMENT_3D('',#20767,#16644,#16645);
#14223=AXIS2_PLACEMENT_3D('',#20769,#16646,#16647);
#14224=AXIS2_PLACEMENT_3D('',#20770,#16648,#16649);
#14225=AXIS2_PLACEMENT_3D('',#20772,#16650,#16651);
#14226=AXIS2_PLACEMENT_3D('',#20774,#16653,#16654);
#14227=AXIS2_PLACEMENT_3D('',#20776,#16655,#16656);
#14228=AXIS2_PLACEMENT_3D('',#20778,#16658,#16659);
#14229=AXIS2_PLACEMENT_3D('',#20780,#16660,#16661);
#14230=AXIS2_PLACEMENT_3D('',#20782,#16663,#16664);
#14231=AXIS2_PLACEMENT_3D('',#20784,#16665,#16666);
#14232=AXIS2_PLACEMENT_3D('',#20785,#16667,#16668);
#14233=AXIS2_PLACEMENT_3D('',#20787,#16669,#16670);
#14234=AXIS2_PLACEMENT_3D('',#20789,#16672,#16673);
#16604=DIRECTION('axis',(0.,0.,1.));
#16605=DIRECTION('refdir',(1.,0.,0.));
#16606=DIRECTION('center_axis',(0.866025403784439,0.,-0.5));
#16607=DIRECTION('ref_axis',(0.5,0.,0.866025403784439));
#16608=DIRECTION('',(-0.5,0.,-0.866025403784439));
#16609=DIRECTION('',(0.,-1.,0.));
#16610=DIRECTION('',(0.5,0.,0.866025403784439));
#16611=DIRECTION('',(0.,-1.,0.));
#16612=DIRECTION('center_axis',(1.20185167898973E-16,0.,-1.));
#16613=DIRECTION('ref_axis',(1.,0.,1.20185167898973E-16));
#16614=DIRECTION('',(-1.,0.,-1.20185167898973E-16));
#16615=DIRECTION('',(0.,-1.,0.));
#16616=DIRECTION('',(1.,0.,1.20185167898973E-16));
#16617=DIRECTION('center_axis',(-0.866025403784439,0.,-0.5));
#16618=DIRECTION('ref_axis',(0.5,0.,-0.866025403784439));
#16619=DIRECTION('',(-0.5,0.,0.866025403784439));
#16620=DIRECTION('',(0.,-1.,0.));
#16621=DIRECTION('',(0.5,0.,-0.866025403784439));
#16622=DIRECTION('center_axis',(-0.866025403784439,0.,0.5));
#16623=DIRECTION('ref_axis',(-0.5,0.,-0.866025403784439));
#16624=DIRECTION('',(0.5,0.,0.866025403784439));
#16625=DIRECTION('',(0.,-1.,0.));
#16626=DIRECTION('',(-0.5,0.,-0.866025403784439));
#16627=DIRECTION('center_axis',(-2.40370335797945E-16,0.,1.));
#16628=DIRECTION('ref_axis',(-1.,0.,-2.40370335797945E-16));
#16629=DIRECTION('',(1.,0.,2.40370335797945E-16));
#16630=DIRECTION('',(0.,-1.,0.));
#16631=DIRECTION('',(-1.,0.,-2.40370335797945E-16));
#16632=DIRECTION('center_axis',(0.866025403784439,0.,0.5));
#16633=DIRECTION('ref_axis',(-0.5,0.,0.866025403784439));
#16634=DIRECTION('',(0.5,0.,-0.866025403784439));
#16635=DIRECTION('',(-0.5,0.,0.866025403784439));
#16636=DIRECTION('center_axis',(0.,1.,0.));
#16637=DIRECTION('ref_axis',(1.,0.,0.));
#16638=DIRECTION('center_axis',(0.,-1.,0.));
#16639=DIRECTION('ref_axis',(0.,0.,-1.));
#16640=DIRECTION('center_axis',(0.,1.,0.));
#16641=DIRECTION('ref_axis',(1.,0.,0.));
#16642=DIRECTION('center_axis',(0.,1.,0.));
#16643=DIRECTION('ref_axis',(1.,0.,0.));
#16644=DIRECTION('center_axis',(0.,1.,0.));
#16645=DIRECTION('ref_axis',(0.,0.,1.));
#16646=DIRECTION('center_axis',(0.,-1.,0.));
#16647=DIRECTION('ref_axis',(1.,0.,0.));
#16648=DIRECTION('center_axis',(0.,-1.,0.));
#16649=DIRECTION('ref_axis',(1.,0.,0.));
#16650=DIRECTION('center_axis',(0.,-1.,0.));
#16651=DIRECTION('ref_axis',(1.,0.,0.));
#16652=DIRECTION('',(0.707106781186548,0.707106781186547,8.65956056235493E-17));
#16653=DIRECTION('center_axis',(0.,-1.,0.));
#16654=DIRECTION('ref_axis',(1.,0.,0.));
#16655=DIRECTION('center_axis',(0.,-1.,0.));
#16656=DIRECTION('ref_axis',(1.,0.,0.));
#16657=DIRECTION('',(0.,1.,0.));
#16658=DIRECTION('center_axis',(0.,1.,0.));
#16659=DIRECTION('ref_axis',(1.,0.,0.));
#16660=DIRECTION('center_axis',(0.,-1.,0.));
#16661=DIRECTION('ref_axis',(1.,0.,0.));
#16662=DIRECTION('',(-0.707106781186547,0.707106781186548,-8.65956056235493E-17));
#16663=DIRECTION('center_axis',(0.,-1.,0.));
#16664=DIRECTION('ref_axis',(0.,0.,-1.));
#16665=DIRECTION('center_axis',(0.,-1.,0.));
#16666=DIRECTION('ref_axis',(1.,0.,0.));
#16667=DIRECTION('center_axis',(0.,1.,0.));
#16668=DIRECTION('ref_axis',(1.,0.,0.));
#16669=DIRECTION('center_axis',(0.,1.,0.));
#16670=DIRECTION('ref_axis',(1.,0.,0.));
#16671=DIRECTION('',(-0.447213595499958,0.894427190999916,-5.47678698264203E-17));
#16672=DIRECTION('center_axis',(0.,-1.,0.));
#16673=DIRECTION('ref_axis',(1.,0.,0.));
#16674=DIRECTION('',(0.,1.,0.));
#20725=CARTESIAN_POINT('',(0.,0.,0.));
#20726=CARTESIAN_POINT('Origin',(0.115470053837925,-0.5,-0.2));
#20727=CARTESIAN_POINT('',(0.23094010767585,-0.5,0.));
#20728=CARTESIAN_POINT('',(0.115470053837925,-0.5,-0.2));
#20729=CARTESIAN_POINT('',(0.23094010767585,-0.5,0.));
#20730=CARTESIAN_POINT('',(0.115470053837925,-0.8,-0.2));
#20731=CARTESIAN_POINT('',(0.115470053837925,-0.5,-0.2));
#20732=CARTESIAN_POINT('',(0.23094010767585,-0.8,0.));
#20733=CARTESIAN_POINT('',(0.23094010767585,-0.8,0.));
#20734=CARTESIAN_POINT('',(0.23094010767585,-0.5,0.));
#20735=CARTESIAN_POINT('Origin',(-0.115470053837925,-0.5,-0.2));
#20736=CARTESIAN_POINT('',(-0.115470053837925,-0.5,-0.2));
#20737=CARTESIAN_POINT('',(0.115470053837925,-0.5,-0.2));
#20738=CARTESIAN_POINT('',(-0.115470053837925,-0.8,-0.2));
#20739=CARTESIAN_POINT('',(-0.115470053837925,-0.5,-0.2));
#20740=CARTESIAN_POINT('',(0.115470053837925,-0.8,-0.2));
#20741=CARTESIAN_POINT('Origin',(-0.23094010767585,-0.5,-2.77555756156289E-17));
#20742=CARTESIAN_POINT('',(-0.23094010767585,-0.5,-2.82820063659975E-17));
#20743=CARTESIAN_POINT('',(-0.115470053837925,-0.5,-0.2));
#20744=CARTESIAN_POINT('',(-0.23094010767585,-0.8,-2.77555756156289E-17));
#20745=CARTESIAN_POINT('',(-0.23094010767585,-0.5,-2.82820063659975E-17));
#20746=CARTESIAN_POINT('',(-0.115470053837925,-0.8,-0.2));
#20747=CARTESIAN_POINT('Origin',(-0.115470053837925,-0.5,0.2));
#20748=CARTESIAN_POINT('',(-0.115470053837925,-0.5,0.2));
#20749=CARTESIAN_POINT('',(-0.23094010767585,-0.5,-2.82820063659975E-17));
#20750=CARTESIAN_POINT('',(-0.115470053837925,-0.8,0.2));
#20751=CARTESIAN_POINT('',(-0.115470053837925,-0.5,0.2));
#20752=CARTESIAN_POINT('',(-0.23094010767585,-0.8,-2.82820063659975E-17));
#20753=CARTESIAN_POINT('Origin',(0.115470053837925,-0.5,0.2));
#20754=CARTESIAN_POINT('',(0.115470053837925,-0.5,0.2));
#20755=CARTESIAN_POINT('',(-0.115470053837925,-0.5,0.2));
#20756=CARTESIAN_POINT('',(0.115470053837925,-0.8,0.2));
#20757=CARTESIAN_POINT('',(0.115470053837925,-0.5,0.2));
#20758=CARTESIAN_POINT('',(-0.115470053837925,-0.8,0.2));
#20759=CARTESIAN_POINT('Origin',(0.23094010767585,-0.5,0.));
#20760=CARTESIAN_POINT('',(0.115470053837925,-0.5,0.2));
#20761=CARTESIAN_POINT('',(0.115470053837925,-0.8,0.2));
#20762=CARTESIAN_POINT('Origin',(0.,-0.5,0.));
#20763=CARTESIAN_POINT('Origin',(0.,-0.8,0.));
#20764=CARTESIAN_POINT('Origin',(0.,-1.8,0.));
#20765=CARTESIAN_POINT('',(-0.24505,-1.8,3.00099698131059E-17));
#20766=CARTESIAN_POINT('Origin',(0.,-1.8,0.));
#20767=CARTESIAN_POINT('Origin',(0.375,0.5,0.));
#20768=CARTESIAN_POINT('',(-0.375,0.5,-4.59242549680257E-17));
#20769=CARTESIAN_POINT('Origin',(0.,0.5,0.));
#20770=CARTESIAN_POINT('Origin',(0.,0.475,0.));
#20771=CARTESIAN_POINT('',(-0.425,0.45,-5.20474889637625E-17));
#20772=CARTESIAN_POINT('Origin',(0.,0.45,0.));
#20773=CARTESIAN_POINT('',(-0.4,0.475,-4.89858719658941E-17));
#20774=CARTESIAN_POINT('Origin',(0.,0.24,0.));
#20775=CARTESIAN_POINT('',(-0.425,0.0299999999999998,-5.20474889637625E-17));
#20776=CARTESIAN_POINT('Origin',(0.,0.0299999999999998,0.));
#20777=CARTESIAN_POINT('',(-0.425,0.24,-5.20474889637625E-17));
#20778=CARTESIAN_POINT('Origin',(0.,0.0150000000000001,0.));
#20779=CARTESIAN_POINT('',(-0.395,4.85722573273506E-17,-4.83735485663204E-17));
#20780=CARTESIAN_POINT('Origin',(0.,0.,0.));
#20781=CARTESIAN_POINT('',(-0.41,0.0150000000000001,-5.02105187650415E-17));
#20782=CARTESIAN_POINT('Origin',(0.27,0.,0.));
#20783=CARTESIAN_POINT('',(-0.27,0.,-3.30654635769785E-17));
#20784=CARTESIAN_POINT('Origin',(0.,0.,0.));
#20785=CARTESIAN_POINT('Origin',(0.,-0.02,0.));
#20786=CARTESIAN_POINT('',(-0.24505,-0.0498999999999999,3.00099698131059E-17));
#20787=CARTESIAN_POINT('Origin',(0.,-0.0498999999999999,0.));
#20788=CARTESIAN_POINT('',(-0.26,-0.02,-3.18408167778312E-17));
#20789=CARTESIAN_POINT('Origin',(0.,-0.995,0.));
#20790=CARTESIAN_POINT('',(-0.24505,-0.995,-3.00099698131059E-17));
#33904=UNCERTAINTY_MEASURE_WITH_UNIT(LENGTH_MEASURE(0.001),#33982,
'DISTANCE_ACCURACY_VALUE',
'Maximum model space distance between geometric entities at asserted c
onnectivities');
#33929=UNCERTAINTY_MEASURE_WITH_UNIT(LENGTH_MEASURE(0.001),#33982,
'DISTANCE_ACCURACY_VALUE',
'Maximum model space distance between geometric entities at asserted c
onnectivities');
#33956=(
GEOMETRIC_REPRESENTATION_CONTEXT(3)
GLOBAL_UNCERTAINTY_ASSIGNED_CONTEXT((#33904))
GLOBAL_UNIT_ASSIGNED_CONTEXT((#33982,#33984,#33985))
REPRESENTATION_CONTEXT('','3D')
);
#33981=(
GEOMETRIC_REPRESENTATION_CONTEXT(3)
GLOBAL_UNCERTAINTY_ASSIGNED_CONTEXT((#33929))
GLOBAL_UNIT_ASSIGNED_CONTEXT((#33982,#33984,#33985))
REPRESENTATION_CONTEXT('','3D')
);
#33982=(
LENGTH_UNIT()
NAMED_UNIT(*)
SI_UNIT(.CENTI.,.METRE.)
);
#33984=(
NAMED_UNIT(*)
PLANE_ANGLE_UNIT()
SI_UNIT($,.RADIAN.)
);
#33985=(
NAMED_UNIT(*)
SI_UNIT($,.STERADIAN.)
SOLID_ANGLE_UNIT()
);
#34012=SHAPE_DEFINITION_REPRESENTATION(#34073,#34208);
#34073=PRODUCT_DEFINITION_SHAPE('',$,#34260);
#34208=SHAPE_REPRESENTATION('',(#14211),#33956);
#34233=PRODUCT_DEFINITION_CONTEXT('part definition',#34388,'design');
#34260=PRODUCT_DEFINITION('M5x18 runner screw','M5x18 runner screw',#34311,
#34233);
#34311=PRODUCT_DEFINITION_FORMATION('',$,#34416);
#34388=APPLICATION_CONTEXT(
'Core Data for Automotive Mechanical Design Process');
#34389=PRODUCT_CONTEXT('part definition',#34388,'mechanical');
#34416=PRODUCT('M5x18 runner screw','M5x18 runner screw',
'M5x18 runner screw',(#34389));
#34518=COLOUR_RGB('Black',0.12,0.14,0.17);
#34519=FILL_AREA_STYLE_COLOUR('',#34518);
#34520=FILL_AREA_STYLE('',(#34519));
#34521=SURFACE_STYLE_FILL_AREA(#34520);
#34522=SURFACE_SIDE_STYLE('',(#34521));
#34523=SURFACE_STYLE_USAGE(.BOTH.,#34522);
#34524=PRESENTATION_STYLE_ASSIGNMENT((#34523));
ENDSEC;
END-ISO-10303-21;
